ISO-10303-21;
HEADER;
FILE_DESCRIPTION (('STEP AP214'),
    '1' );
FILE_NAME ('End Cap Ring.step',
    '2026-10-06T14:00:01',
    ( '' ),
    ( '' ),
    'SwSTEP 2.0',
    'SolidWorks 2020',
    '' );
FILE_SCHEMA (( 'AUTOMOTIVE_DESIGN' ));
ENDSEC;

DATA;
#153=CARTESIAN_POINT ( 'NONE',  ( 68.00000000000001421, -1.025519176787267142E-28, -7.122621931239990530E-13 ) ) ;
#229=DIRECTION ( 'NONE',  ( -1.000000000000000000, 0.000000000000000000, 1.047444401652940007E-14 ) ) ;
#356=DIRECTION ( 'NONE',  ( 1.047444401652940007E-14, 0.000000000000000000, 1.000000000000000000 ) ) ;
#452=AXIS2_PLACEMENT_3D ( 'NONE', #22650, #10741, #10597 ) ;
#463=CARTESIAN_POINT ( 'NONE',  ( 65.04999999999996874, -1.025519176787267142E-28, -4.100000000000681766 ) ) ;
#504=CARTESIAN_POINT ( 'NONE',  ( 64.99999999999997158, -1.025519176787267142E-28, -3.500000000000680345 ) ) ;
#538=FACE_OUTER_BOUND ( 'NONE', #16964, .T. ) ;
#584=CARTESIAN_POINT ( 'NONE',  ( 65.00000000000001421, -1.025519176787267142E-28, -6.808388610744108654E-13 ) ) ;
#637=SHAPE_REPRESENTATION_RELATIONSHIP ( 'NONE' , 'NONE' ,  #27890, #14241 ) ;
#667=CARTESIAN_POINT ( 'NONE',  ( 67.95000000000005969, -1.025519176787267142E-28, 4.049999999999288391 ) ) ;
#1021=EDGE_CURVE ( 'NONE', #10599, #1198, #21966, .T. ) ;
#1064=CARTESIAN_POINT ( 'NONE',  ( 65.00000000000005684, 4.286263797014729811E-16, 3.499999999999318767 ) ) ;
#1198=VERTEX_POINT ( 'NONE', #9264 ) ;
#1567=STYLED_ITEM ( 'NONE', ( #16134 ), #4661 ) ;
#1589=ORIENTED_EDGE ( 'NONE', *, *, #9009, .F. ) ;
#1606=EDGE_CURVE ( 'NONE', #27342, #25393, #17410, .T. ) ;
#1715=CARTESIAN_POINT ( 'NONE',  ( 68.00000000000001421, -1.025519176787267142E-28, -7.122621931239990530E-13 ) ) ;
#1777=DIRECTION ( 'NONE',  ( -1.000000000000000000, 0.000000000000000000, 1.047444401652940007E-14 ) ) ;
#1866=DIRECTION ( 'NONE',  ( 1.000000000000000000, -0.000000000000000000, -1.047444401652940007E-14 ) ) ;
#1991=CIRCLE ( 'NONE', #12599, 3.499999999999999556 ) ;
#2201=ORIENTED_EDGE ( 'NONE', *, *, #1606, .T. ) ;
#2252=CARTESIAN_POINT ( 'NONE',  ( 67.99999999999997158, -1.025519176787267142E-28, -3.500000000000711875 ) ) ;
#2429=CARTESIAN_POINT ( 'NONE',  ( 67.95000000000003126, -1.025519176787267142E-28, -7.117384709231726808E-13 ) ) ;
#2461=CARTESIAN_POINT ( 'NONE',  ( 65.00000000000001421, -1.025519176787267142E-28, -6.808388610744108654E-13 ) ) ;
#2481=ORIENTED_EDGE ( 'NONE', *, *, #22900, .F. ) ;
#2496=AXIS2_PLACEMENT_3D ( 'NONE', #29793, #8107, #17776 ) ;
#2614=FACE_BOUND ( 'NONE', #11778, .T. ) ;
#2698=DIRECTION ( 'NONE',  ( 1.000000000000000000, -0.000000000000000000, -1.047444401652940007E-14 ) ) ;
#2710=ORIENTED_EDGE ( 'NONE', *, *, #10733, .T. ) ;
#2783=DIRECTION ( 'NONE',  ( 1.027984282060330001E-14, 0.000000000000000000, 1.000000000000000000 ) ) ;
#2841=UNCERTAINTY_MEASURE_WITH_UNIT (LENGTH_MEASURE( 1.000000000000000082E-05 ), #22345, 'distance_accuracy_value', 'NONE');
#2938=VERTEX_POINT ( 'NONE', #11020 ) ;
#3057=AXIS2_PLACEMENT_3D ( 'NONE', #23501, #8930, #28259 ) ;
#3335=ORIENTED_EDGE ( 'NONE', *, *, #15472, .F. ) ;
#3651=DIRECTION ( 'NONE',  ( 1.000000000000000000, -0.000000000000000000, -1.047444401652940007E-14 ) ) ;
#3726=CARTESIAN_POINT ( 'NONE',  ( 64.99999999999997158, -1.025519176787267142E-28, -3.500000000000680345 ) ) ;
#4028=VERTEX_POINT ( 'NONE', #8563 ) ;
#4114=DIRECTION ( 'NONE',  ( -1.000000000000000000, 0.000000000000000000, 1.047444401652940007E-14 ) ) ;
#4358=VERTEX_POINT ( 'NONE', #21097 ) ;
#4410=( LENGTH_UNIT ( ) NAMED_UNIT ( * ) SI_UNIT ( .MILLI., .METRE. ) );
#4544=CARTESIAN_POINT ( 'NONE',  ( 65.00000000000001421, -1.025519176787267142E-28, -6.808388610744108654E-13 ) ) ;
#4567=FILL_AREA_STYLE_COLOUR ( '', #21336 ) ;
#4661=MANIFOLD_SOLID_BREP ( 'Stock-MAS-683-1', #8946 ) ;
#4739=DIRECTION ( 'NONE',  ( 1.027984282060330001E-14, 0.000000000000000000, 1.000000000000000000 ) ) ;
#4857=CARTESIAN_POINT ( 'NONE',  ( 65.05000000000005400, -1.025519176787267142E-28, 4.049999999999318590 ) ) ;
#4963=CARTESIAN_POINT ( 'NONE',  ( 65.00000000000005684, 5.021051876503122852E-16, 4.099999999999319300 ) ) ;
#5089=FILL_AREA_STYLE ('',( #19670 ) ) ;
#5354=TOROIDAL_SURFACE ( 'NONE', #14444, 4.050000000000000711, 0.05000000000000000278 ) ;
#5516=COLOUR_RGB ( '', 0.66274510, 0.83137255, 0.94901961) ;
#5629=ORIENTED_EDGE ( 'NONE', *, *, #23923, .F. ) ;
#5746=PLANE ( 'NONE',  #24814 ) ;
#5761=DIRECTION ( 'NONE',  ( -1.000000000000000000, 0.000000000000000000, 1.047444401652940007E-14 ) ) ;
#5775=EDGE_LOOP ( 'NONE', ( #17243, #15702 ) ) ;
#5874=AXIS2_PLACEMENT_3D ( 'NONE', #12829, #17613, #10312 ) ;
#5961=AXIS2_PLACEMENT_3D ( 'NONE', #8989, #12001, #31305 ) ;
#6025=( GEOMETRIC_REPRESENTATION_CONTEXT ( 3 ) GLOBAL_UNCERTAINTY_ASSIGNED_CONTEXT ( ( #22182 ) ) GLOBAL_UNIT_ASSIGNED_CONTEXT ( ( #19816, #24401, #28997 ) ) REPRESENTATION_CONTEXT ( 'NONE', 'WORKASPACE' ) );
#6033=PRODUCT_CONTEXT ( 'NONE', #22700, 'mechanical' ) ;
#6362=ORIENTED_EDGE ( 'NONE', *, *, #16089, .T. ) ;
#6469=AXIS2_PLACEMENT_3D ( 'NONE', #4857, #9479, #14042 ) ;
#6595=ORIENTED_EDGE ( 'NONE', *, *, #10298, .F. ) ;
#6799=ADVANCED_FACE ( 'NONE', ( #21025 ), #26236, .T. ) ;
#7130=DIRECTION ( 'NONE',  ( 1.000000000000000000, -0.000000000000000000, -1.047444401652940007E-14 ) ) ;
#7247=EDGE_LOOP ( 'NONE', ( #2201, #16881 ) ) ;
#7269=DIRECTION ( 'NONE',  ( -1.000000000000000000, 0.000000000000000000, 1.047444401652940007E-14 ) ) ;
#7364=ADVANCED_FACE ( 'NONE', ( #16864 ), #13637, .T. ) ;
#7606=UNCERTAINTY_MEASURE_WITH_UNIT (LENGTH_MEASURE( 1.000000000000000082E-05 ), #4410, 'distance_accuracy_value', 'NONE');
#7622=ORIENTED_EDGE ( 'NONE', *, *, #11765, .F. ) ;
#7649=CARTESIAN_POINT ( 'NONE',  ( 67.99999999999997158, 4.990435706524438473E-16, -4.050000000000713030 ) ) ;
#7657=ADVANCED_FACE ( 'NONE', ( #15572, #21238 ), #5746, .F. ) ;
#7669=DIRECTION ( 'NONE',  ( 1.189524669241239263E-14, 0.000000000000000000, 1.000000000000000000 ) ) ;
#7746=CARTESIAN_POINT ( 'NONE',  ( 65.00000000000001421, -1.025519176787267142E-28, -6.808388610744108654E-13 ) ) ;
#7819=ORIENTED_EDGE ( 'NONE', *, *, #10733, .F. ) ;
#7903=ORIENTED_EDGE ( 'NONE', *, *, #17400, .F. ) ;
#8024=CARTESIAN_POINT ( 'NONE',  ( 65.05000000000005400, 5.021051876503140601E-16, 4.099999999999318412 ) ) ;
#8107=DIRECTION ( 'NONE',  ( 1.000000000000000000, -0.000000000000000000, -1.047444401652940007E-14 ) ) ;
#8181=DIRECTION ( 'NONE',  ( 1.027984282060330001E-14, 0.000000000000000000, 1.000000000000000000 ) ) ;
#8420=EDGE_CURVE ( 'NONE', #4028, #4358, #24846, .T. ) ;
#8482=EDGE_CURVE ( 'NONE', #18265, #22989, #15754, .T. ) ;
#8563=CARTESIAN_POINT ( 'NONE',  ( 64.99999999999997158, 4.990435706524439459E-16, -4.050000000000681943 ) ) ;
#8827=DIRECTION ( 'NONE',  ( 1.189524669241239263E-14, 0.000000000000000000, 1.000000000000000000 ) ) ;
#8877=ORIENTED_EDGE ( 'NONE', *, *, #1021, .F. ) ;
#8930=DIRECTION ( 'NONE',  ( -1.000000000000000000, 0.000000000000000000, 1.047444401652940007E-14 ) ) ;
#8946=CLOSED_SHELL ( 'NONE', ( #19391, #20297, #21050, #11430, #25856, #7657, #6799, #11241, #7364, #25289 ) ) ;
#8989=CARTESIAN_POINT ( 'NONE',  ( 67.95000000000003126, -1.025519176787267142E-28, -7.117384709231726808E-13 ) ) ;
#9009=EDGE_CURVE ( 'NONE', #23673, #25393, #9519, .T. ) ;
#9018=AXIS2_PLACEMENT_3D ( 'NONE', #25987, #9060, #11596 ) ;
#9060=DIRECTION ( 'NONE',  ( 0.000000000000000000, 0.000000000000000000, 1.000000000000000000 ) ) ;
#9185=MECHANICAL_DESIGN_GEOMETRIC_PRESENTATION_REPRESENTATION('',(#1567),#30916);
#9264=CARTESIAN_POINT ( 'NONE',  ( 67.94999999999998863, -1.025519176787267142E-28, -4.100000000000712852 ) ) ;
#9321=SURFACE_STYLE_FILL_AREA ( #11368 ) ;
#9455=ORIENTED_EDGE ( 'NONE', *, *, #11244, .F. ) ;
#9479=DIRECTION ( 'NONE',  ( 0.000000000000000000, -1.000000000000000000, 0.000000000000000000 ) ) ;
#9519=LINE ( 'NONE', #25956, #24616 ) ;
#9725=DIRECTION ( 'NONE',  ( 1.000000000000000000, -0.000000000000000000, -1.047444401652940007E-14 ) ) ;
#9819=PRODUCT_DEFINITION_CONTEXT ( 'detailed design', #26389, 'design' ) ;
#10007=AXIS2_PLACEMENT_3D ( 'NONE', #21139, #1777, #8181 ) ;
#10163=ORIENTED_EDGE ( 'NONE', *, *, #11765, .T. ) ;
#10197=PLANE ( 'NONE',  #10454 ) ;
#10298=EDGE_CURVE ( 'NONE', #26730, #27342, #24723, .T. ) ;
#10308=PRODUCT ( 'End Cap Ring', 'End Cap Ring', '', ( #6033 ) ) ;
#10312=DIRECTION ( 'NONE',  ( 1.047444401652940007E-14, 0.000000000000000000, 1.000000000000000000 ) ) ;
#10454=AXIS2_PLACEMENT_3D ( 'NONE', #2461, #229, #19866 ) ;
#10474=CIRCLE ( 'NONE', #14522, 0.04999999999999969746 ) ;
#10488=FACE_OUTER_BOUND ( 'NONE', #15748, .T. ) ;
#10597=DIRECTION ( 'NONE',  ( 0.000000000000000000, -1.224646799147353947E-16, 1.000000000000000000 ) ) ;
#10599=VERTEX_POINT ( 'NONE', #463 ) ;
#10733=EDGE_CURVE ( 'NONE', #10599, #4028, #22210, .T. ) ;
#10741=DIRECTION ( 'NONE',  ( 1.282749433769087582E-30, 1.000000000000000000, 1.224646799147353207E-16 ) ) ;
#10884=TOROIDAL_SURFACE ( 'NONE', #16987, 4.050000000000000711, 0.05000000000000000278 ) ;
#10942=DIRECTION ( 'NONE',  ( -1.000000000000000000, 0.000000000000000000, 1.047444401652940007E-14 ) ) ;
#11020=CARTESIAN_POINT ( 'NONE',  ( 67.95000000000005969, 5.021051876503122852E-16, 4.099999999999288214 ) ) ;
#11086=CARTESIAN_POINT ( 'NONE',  ( 67.95000000000003126, -1.025519176787267142E-28, -7.117384709231726808E-13 ) ) ;
#11159=DIRECTION ( 'NONE',  ( 1.027984282060330001E-14, 0.000000000000000000, 1.000000000000000000 ) ) ;
#11241=ADVANCED_FACE ( 'NONE', ( #10488 ), #20163, .F. ) ;
#11244=EDGE_CURVE ( 'NONE', #25393, #27342, #1991, .T. ) ;
#11283=CARTESIAN_POINT ( 'NONE',  ( 65.05000000000001137, -1.025519176787267142E-28, -6.813625832752373386E-13 ) ) ;
#11368=FILL_AREA_STYLE ('',( #4567 ) ) ;
#11399=CIRCLE ( 'NONE', #25050, 4.100000000000000533 ) ;
#11430=ADVANCED_FACE ( 'NONE', ( #12337 ), #29586, .T. ) ;
#11596=DIRECTION ( 'NONE',  ( 1.000000000000000000, 0.000000000000000000, 0.000000000000000000 ) ) ;
#11620=PRODUCT_DEFINITION_FORMATION_WITH_SPECIFIED_SOURCE ( 'ANY', '', #10308, .NOT_KNOWN. ) ;
#11651=PRODUCT_DEFINITION ( 'UNKNOWN', '', #11620, #9819 ) ;
#11669=ORIENTED_EDGE ( 'NONE', *, *, #26819, .F. ) ;
#11745=ORIENTED_EDGE ( 'NONE', *, *, #16089, .F. ) ;
#11765=EDGE_CURVE ( 'NONE', #26730, #23673, #20228, .T. ) ;
#11778=EDGE_LOOP ( 'NONE', ( #7622, #3335 ) ) ;
#11878=DIRECTION ( 'NONE',  ( 1.000000000000000000, -0.000000000000000000, -1.047444401652940007E-14 ) ) ;
#12001=DIRECTION ( 'NONE',  ( -1.000000000000000000, 0.000000000000000000, 1.047444401652940007E-14 ) ) ;
#12070=( NAMED_UNIT ( * ) PLANE_ANGLE_UNIT ( ) SI_UNIT ( $, .RADIAN. ) );
#12104=AXIS2_PLACEMENT_3D ( 'NONE', #7746, #2698, #12650 ) ;
#12337=FACE_OUTER_BOUND ( 'NONE', #19887, .T. ) ;
#12428=EDGE_LOOP ( 'NONE', ( #11745, #2710, #16627, #28611 ) ) ;
#12467=ORIENTED_EDGE ( 'NONE', *, *, #22900, .T. ) ;
#12599=AXIS2_PLACEMENT_3D ( 'NONE', #27417, #10942, #17923 ) ;
#12650=DIRECTION ( 'NONE',  ( -1.015447888376667464E-14, 0.000000000000000000, -1.000000000000000000 ) ) ;
#12824=PRODUCT_DEFINITION_SHAPE ( 'NONE', 'NONE',  #11651 ) ;
#12829=CARTESIAN_POINT ( 'NONE',  ( 65.05000000000001137, -1.025519176787267142E-28, -6.813625832752373386E-13 ) ) ;
#12997=CARTESIAN_POINT ( 'NONE',  ( 68.00000000000005684, -1.025519176787267142E-28, 4.049999999999288391 ) ) ;
#13353=EDGE_LOOP ( 'NONE', ( #5629, #28468, #18032, #24072 ) ) ;
#13637=TOROIDAL_SURFACE ( 'NONE', #3057, 4.050000000000000711, 0.05000000000000000278 ) ;
#13676=ORIENTED_EDGE ( 'NONE', *, *, #8420, .F. ) ;
#13724=DIRECTION ( 'NONE',  ( 1.015447888376667464E-14, 0.000000000000000000, 1.000000000000000000 ) ) ;
#13799=ORIENTED_EDGE ( 'NONE', *, *, #9009, .T. ) ;
#14042=DIRECTION ( 'NONE',  ( 0.000000000000000000, 0.000000000000000000, -1.000000000000000000 ) ) ;
#14193=DIRECTION ( 'NONE',  ( 1.000000000000000000, -0.000000000000000000, -1.047444401652940007E-14 ) ) ;
#14241=ADVANCED_BREP_SHAPE_REPRESENTATION ( '', ( #4661, #9018 ), #25740 ) ;
#14422=SURFACE_STYLE_USAGE ( .BOTH. , #29308 ) ;
#14444=AXIS2_PLACEMENT_3D ( 'NONE', #11283, #28245, #22878 ) ;
#14461=AXIS2_PLACEMENT_3D ( 'NONE', #11086, #4114, #16315 ) ;
#14473=VECTOR ( 'NONE', #17151, 1000.000000000000000 ) ;
#14522=AXIS2_PLACEMENT_3D ( 'NONE', #17997, #27648, #23223 ) ;
#14776=ORIENTED_EDGE ( 'NONE', *, *, #28854, .F. ) ;
#14810=CARTESIAN_POINT ( 'NONE',  ( 64.99999999999997158, -1.025519176787267142E-28, -4.100000000000680878 ) ) ;
#15131=VERTEX_POINT ( 'NONE', #8024 ) ;
#15151=DIRECTION ( 'NONE',  ( 1.000000000000000000, -0.000000000000000000, -1.047444401652940007E-14 ) ) ;
#15306=FACE_OUTER_BOUND ( 'NONE', #25401, .T. ) ;
#15472=EDGE_CURVE ( 'NONE', #23673, #26730, #15489, .T. ) ;
#15489=CIRCLE ( 'NONE', #16509, 3.499999999999999556 ) ;
#15557=CIRCLE ( 'NONE', #6469, 0.04999999999999969746 ) ;
#15572=FACE_OUTER_BOUND ( 'NONE', #5775, .T. ) ;
#15702=ORIENTED_EDGE ( 'NONE', *, *, #19683, .T. ) ;
#15748=EDGE_LOOP ( 'NONE', ( #1589, #19744, #24781, #9455 ) ) ;
#15754=CIRCLE ( 'NONE', #28906, 4.050000000000000711 ) ;
#15857=ORIENTED_EDGE ( 'NONE', *, *, #28854, .T. ) ;
#15975=SHAPE_DEFINITION_REPRESENTATION ( #12824, #27890 ) ;
#16089=EDGE_CURVE ( 'NONE', #10599, #15131, #19578, .T. ) ;
#16134=PRESENTATION_STYLE_ASSIGNMENT (( #30373 ) ) ;
#16140=STYLED_ITEM ( 'NONE', ( #21896 ), #14241 ) ;
#16293=SURFACE_SIDE_STYLE ('',( #9321 ) ) ;
#16315=DIRECTION ( 'NONE',  ( 1.015447888376667464E-14, 0.000000000000000000, 1.000000000000000000 ) ) ;
#16509=AXIS2_PLACEMENT_3D ( 'NONE', #26974, #5761, #7669 ) ;
#16627=ORIENTED_EDGE ( 'NONE', *, *, #29026, .F. ) ;
#16864=FACE_OUTER_BOUND ( 'NONE', #24576, .T. ) ;
#16881=ORIENTED_EDGE ( 'NONE', *, *, #11244, .T. ) ;
#16964=EDGE_LOOP ( 'NONE', ( #23893, #21527 ) ) ;
#16987=AXIS2_PLACEMENT_3D ( 'NONE', #2429, #22060, #356 ) ;
#17151=DIRECTION ( 'NONE',  ( 1.000000000000000000, -0.000000000000000000, -1.047444401652940007E-14 ) ) ;
#17243=ORIENTED_EDGE ( 'NONE', *, *, #8482, .T. ) ;
#17400=EDGE_CURVE ( 'NONE', #1198, #2938, #22561, .T. ) ;
#17410=CIRCLE ( 'NONE', #22976, 3.499999999999999556 ) ;
#17561=DIRECTION ( 'NONE',  ( 1.189524669241239263E-14, 0.000000000000000000, 1.000000000000000000 ) ) ;
#17613=DIRECTION ( 'NONE',  ( -1.000000000000000000, 0.000000000000000000, 1.047444401652940007E-14 ) ) ;
#17631=ORIENTED_EDGE ( 'NONE', *, *, #1606, .F. ) ;
#17776=DIRECTION ( 'NONE',  ( -1.189524669241239263E-14, 0.000000000000000000, -1.000000000000000000 ) ) ;
#17923=DIRECTION ( 'NONE',  ( 1.189524669241239263E-14, 0.000000000000000000, 1.000000000000000000 ) ) ;
#17997=CARTESIAN_POINT ( 'NONE',  ( 67.94999999999998863, 4.959819536545755081E-16, -4.050000000000713030 ) ) ;
#18032=ORIENTED_EDGE ( 'NONE', *, *, #1021, .T. ) ;
#18265=VERTEX_POINT ( 'NONE', #12997 ) ;
#18435=FACE_OUTER_BOUND ( 'NONE', #24591, .T. ) ;
#18757=EDGE_CURVE ( 'NONE', #15131, #10599, #11399, .T. ) ;
#18818=AXIS2_PLACEMENT_3D ( 'NONE', #29240, #22280, #2783 ) ;
#18908=CARTESIAN_POINT ( 'NONE',  ( 68.00000000000005684, 4.286263797014710090E-16, 3.499999999999287681 ) ) ;
#19376=FACE_OUTER_BOUND ( 'NONE', #25425, .T. ) ;
#19391=ADVANCED_FACE ( 'NONE', ( #22511 ), #19546, .T. ) ;
#19546=TOROIDAL_SURFACE ( 'NONE', #5874, 4.050000000000000711, 0.05000000000000000278 ) ;
#19547=DIRECTION ( 'NONE',  ( 0.000000000000000000, 0.000000000000000000, -1.000000000000000000 ) ) ;
#19571=CIRCLE ( 'NONE', #31192, 4.050000000000000711 ) ;
#19578=CIRCLE ( 'NONE', #30171, 4.100000000000000533 ) ;
#19670=FILL_AREA_STYLE_COLOUR ( '', #5516 ) ;
#19683=EDGE_CURVE ( 'NONE', #22989, #18265, #19571, .T. ) ;
#19744=ORIENTED_EDGE ( 'NONE', *, *, #15472, .T. ) ;
#19816=( LENGTH_UNIT ( ) NAMED_UNIT ( * ) SI_UNIT ( .MILLI., .METRE. ) );
#19866=DIRECTION ( 'NONE',  ( 1.047444401652940007E-14, 0.000000000000000000, 1.000000000000000000 ) ) ;
#19887=EDGE_LOOP ( 'NONE', ( #6362, #30351, #15857, #8877 ) ) ;
#20163=CYLINDRICAL_SURFACE ( 'NONE', #2496, 3.499999999999999556 ) ;
#20228=CIRCLE ( 'NONE', #26288, 3.499999999999999556 ) ;
#20297=ADVANCED_FACE ( 'NONE', ( #19376 ), #10884, .T. ) ;
#20430=AXIS2_PLACEMENT_3D ( 'NONE', #584, #15151, #29718 ) ;
#21025=FACE_OUTER_BOUND ( 'NONE', #13353, .T. ) ;
#21050=ADVANCED_FACE ( 'NONE', ( #15306 ), #24807, .F. ) ;
#21097=CARTESIAN_POINT ( 'NONE',  ( 65.00000000000005684, -1.025519176787267142E-28, 4.049999999999319478 ) ) ;
#21139=CARTESIAN_POINT ( 'NONE',  ( 65.00000000000001421, -1.025519176787267142E-28, -6.808388610744108654E-13 ) ) ;
#21206=MECHANICAL_DESIGN_GEOMETRIC_PRESENTATION_REPRESENTATION('',(#16140),#6025);
#21238=FACE_BOUND ( 'NONE', #7247, .T. ) ;
#21336=COLOUR_RGB ( '', 0.66274510, 0.83137255, 0.94901961) ;
#21514=AXIS2_PLACEMENT_3D ( 'NONE', #667, #26812, #19547 ) ;
#21527=ORIENTED_EDGE ( 'NONE', *, *, #8420, .T. ) ;
#21896=PRESENTATION_STYLE_ASSIGNMENT (( #14422 ) ) ;
#21966=LINE ( 'NONE', #14810, #29932 ) ;
#22060=DIRECTION ( 'NONE',  ( -1.000000000000000000, 0.000000000000000000, 1.047444401652940007E-14 ) ) ;
#22182=UNCERTAINTY_MEASURE_WITH_UNIT (LENGTH_MEASURE( 1.000000000000000082E-05 ), #19816, 'distance_accuracy_value', 'NONE');
#22210=CIRCLE ( 'NONE', #452, 0.04999999999999969746 ) ;
#22280=DIRECTION ( 'NONE',  ( -1.000000000000000000, 0.000000000000000000, 1.047444401652940007E-14 ) ) ;
#22340=ORIENTED_EDGE ( 'NONE', *, *, #26819, .T. ) ;
#22345=( LENGTH_UNIT ( ) NAMED_UNIT ( * ) SI_UNIT ( .MILLI., .METRE. ) );
#22511=FACE_OUTER_BOUND ( 'NONE', #12428, .T. ) ;
#22561=CIRCLE ( 'NONE', #14461, 4.100000000000000533 ) ;
#22650=CARTESIAN_POINT ( 'NONE',  ( 65.04999999999996874, 4.959819536545755081E-16, -4.050000000000682832 ) ) ;
#22700=APPLICATION_CONTEXT ( 'automotive_design' ) ;
#22878=DIRECTION ( 'NONE',  ( 1.047444401652940007E-14, 0.000000000000000000, 1.000000000000000000 ) ) ;
#22900=EDGE_CURVE ( 'NONE', #18265, #2938, #28574, .T. ) ;
#22976=AXIS2_PLACEMENT_3D ( 'NONE', #153, #7269, #17561 ) ;
#22989=VERTEX_POINT ( 'NONE', #7649 ) ;
#23223=DIRECTION ( 'NONE',  ( 0.000000000000000000, -1.224646799147353947E-16, 1.000000000000000000 ) ) ;
#23407=DIRECTION ( 'NONE',  ( 1.015447888376667464E-14, 0.000000000000000000, 1.000000000000000000 ) ) ;
#23501=CARTESIAN_POINT ( 'NONE',  ( 67.95000000000003126, -1.025519176787267142E-28, -7.117384709231726808E-13 ) ) ;
#23673=VERTEX_POINT ( 'NONE', #1064 ) ;
#23774=CARTESIAN_POINT ( 'NONE',  ( 68.00000000000001421, -1.025519176787267142E-28, -7.122621931239990530E-13 ) ) ;
#23822=LINE ( 'NONE', #4963, #25925 ) ;
#23890=( NAMED_UNIT ( * ) PLANE_ANGLE_UNIT ( ) SI_UNIT ( $, .RADIAN. ) );
#23893=ORIENTED_EDGE ( 'NONE', *, *, #29026, .T. ) ;
#23923=EDGE_CURVE ( 'NONE', #15131, #2938, #23822, .T. ) ;
#24072=ORIENTED_EDGE ( 'NONE', *, *, #17400, .T. ) ;
#24178=CIRCLE ( 'NONE', #5961, 4.100000000000000533 ) ;
#24184=DIRECTION ( 'NONE',  ( 1.000000000000000000, -0.000000000000000000, -1.047444401652940007E-14 ) ) ;
#24401=( NAMED_UNIT ( * ) PLANE_ANGLE_UNIT ( ) SI_UNIT ( $, .RADIAN. ) );
#24576=EDGE_LOOP ( 'NONE', ( #11669, #30980, #12467, #7903 ) ) ;
#24591=EDGE_LOOP ( 'NONE', ( #7819, #27212, #28916, #13676 ) ) ;
#24616=VECTOR ( 'NONE', #7130, 1000.000000000000000 ) ;
#24723=LINE ( 'NONE', #504, #14473 ) ;
#24781=ORIENTED_EDGE ( 'NONE', *, *, #10298, .T. ) ;
#24807=CYLINDRICAL_SURFACE ( 'NONE', #20430, 3.499999999999999556 ) ;
#24814=AXIS2_PLACEMENT_3D ( 'NONE', #1715, #28493, #25047 ) ;
#24846=CIRCLE ( 'NONE', #18818, 4.050000000000000711 ) ;
#25047=DIRECTION ( 'NONE',  ( 1.047444401652940007E-14, 0.000000000000000000, 1.000000000000000000 ) ) ;
#25050=AXIS2_PLACEMENT_3D ( 'NONE', #28145, #1866, #23407 ) ;
#25257=DIRECTION ( 'NONE',  ( 1.000000000000000000, -0.000000000000000000, -1.047444401652940007E-14 ) ) ;
#25289=ADVANCED_FACE ( 'NONE', ( #18435 ), #5354, .T. ) ;
#25345=CARTESIAN_POINT ( 'NONE',  ( 65.05000000000001137, -1.025519176787267142E-28, -6.813625832752373386E-13 ) ) ;
#25393=VERTEX_POINT ( 'NONE', #18908 ) ;
#25401=EDGE_LOOP ( 'NONE', ( #10163, #13799, #17631, #6595 ) ) ;
#25425=EDGE_LOOP ( 'NONE', ( #27495, #22340, #14776, #2481 ) ) ;
#25560=CARTESIAN_POINT ( 'NONE',  ( 68.00000000000001421, -1.025519176787267142E-28, -7.122621931239990530E-13 ) ) ;
#25740=( GEOMETRIC_REPRESENTATION_CONTEXT ( 3 ) GLOBAL_UNCERTAINTY_ASSIGNED_CONTEXT ( ( #2841 ) ) GLOBAL_UNIT_ASSIGNED_CONTEXT ( ( #22345, #12070, #26622 ) ) REPRESENTATION_CONTEXT ( 'NONE', 'WORKASPACE' ) );
#25771=AXIS2_PLACEMENT_3D ( 'NONE', #4544, #14193, #28612 ) ;
#25856=ADVANCED_FACE ( 'NONE', ( #538, #2614 ), #10197, .T. ) ;
#25925=VECTOR ( 'NONE', #9725, 1000.000000000000000 ) ;
#25956=CARTESIAN_POINT ( 'NONE',  ( 65.00000000000005684, 4.286263797014710090E-16, 3.499999999999318767 ) ) ;
#25987=CARTESIAN_POINT ( 'NONE',  ( 0.000000000000000000, 0.000000000000000000, 0.000000000000000000 ) ) ;
#26236=CYLINDRICAL_SURFACE ( 'NONE', #25771, 4.100000000000000533 ) ;
#26288=AXIS2_PLACEMENT_3D ( 'NONE', #28640, #31162, #8827 ) ;
#26389=APPLICATION_CONTEXT ( 'automotive_design' ) ;
#26622=( NAMED_UNIT ( * ) SI_UNIT ( $, .STERADIAN. ) SOLID_ANGLE_UNIT ( ) );
#26730=VERTEX_POINT ( 'NONE', #3726 ) ;
#26812=DIRECTION ( 'NONE',  ( 0.000000000000000000, -1.000000000000000000, 0.000000000000000000 ) ) ;
#26819=EDGE_CURVE ( 'NONE', #22989, #1198, #10474, .T. ) ;
#26974=CARTESIAN_POINT ( 'NONE',  ( 65.00000000000001421, -1.025519176787267142E-28, -6.808388610744108654E-13 ) ) ;
#27072=SURFACE_STYLE_FILL_AREA ( #5089 ) ;
#27190=CIRCLE ( 'NONE', #10007, 4.050000000000000711 ) ;
#27212=ORIENTED_EDGE ( 'NONE', *, *, #18757, .F. ) ;
#27342=VERTEX_POINT ( 'NONE', #2252 ) ;
#27417=CARTESIAN_POINT ( 'NONE',  ( 68.00000000000001421, -1.025519176787267142E-28, -7.122621931239990530E-13 ) ) ;
#27495=ORIENTED_EDGE ( 'NONE', *, *, #19683, .F. ) ;
#27648=DIRECTION ( 'NONE',  ( 1.282749433769087582E-30, 1.000000000000000000, 1.224646799147353207E-16 ) ) ;
#27890=SHAPE_REPRESENTATION ( 'End Cap Ring', ( #9018 ), #25740 ) ;
#28145=CARTESIAN_POINT ( 'NONE',  ( 65.05000000000001137, -1.025519176787267142E-28, -6.813625832752373386E-13 ) ) ;
#28245=DIRECTION ( 'NONE',  ( -1.000000000000000000, 0.000000000000000000, 1.047444401652940007E-14 ) ) ;
#28259=DIRECTION ( 'NONE',  ( 1.047444401652940007E-14, 0.000000000000000000, 1.000000000000000000 ) ) ;
#28468=ORIENTED_EDGE ( 'NONE', *, *, #18757, .T. ) ;
#28493=DIRECTION ( 'NONE',  ( -1.000000000000000000, 0.000000000000000000, 1.047444401652940007E-14 ) ) ;
#28574=CIRCLE ( 'NONE', #21514, 0.04999999999999969746 ) ;
#28611=ORIENTED_EDGE ( 'NONE', *, *, #28851, .F. ) ;
#28612=DIRECTION ( 'NONE',  ( -1.015447888376667464E-14, 0.000000000000000000, -1.000000000000000000 ) ) ;
#28638=( NAMED_UNIT ( * ) SI_UNIT ( $, .STERADIAN. ) SOLID_ANGLE_UNIT ( ) );
#28640=CARTESIAN_POINT ( 'NONE',  ( 65.00000000000001421, -1.025519176787267142E-28, -6.808388610744108654E-13 ) ) ;
#28851=EDGE_CURVE ( 'NONE', #15131, #4358, #15557, .T. ) ;
#28854=EDGE_CURVE ( 'NONE', #2938, #1198, #24178, .T. ) ;
#28906=AXIS2_PLACEMENT_3D ( 'NONE', #25560, #25257, #11159 ) ;
#28916=ORIENTED_EDGE ( 'NONE', *, *, #28851, .T. ) ;
#28997=( NAMED_UNIT ( * ) SI_UNIT ( $, .STERADIAN. ) SOLID_ANGLE_UNIT ( ) );
#29026=EDGE_CURVE ( 'NONE', #4358, #4028, #27190, .T. ) ;
#29240=CARTESIAN_POINT ( 'NONE',  ( 65.00000000000001421, -1.025519176787267142E-28, -6.808388610744108654E-13 ) ) ;
#29308=SURFACE_SIDE_STYLE ('',( #27072 ) ) ;
#29586=CYLINDRICAL_SURFACE ( 'NONE', #12104, 4.100000000000000533 ) ;
#29718=DIRECTION ( 'NONE',  ( -1.189524669241239263E-14, 0.000000000000000000, -1.000000000000000000 ) ) ;
#29793=CARTESIAN_POINT ( 'NONE',  ( 65.00000000000001421, -1.025519176787267142E-28, -6.808388610744108654E-13 ) ) ;
#29932=VECTOR ( 'NONE', #24184, 1000.000000000000000 ) ;
#30171=AXIS2_PLACEMENT_3D ( 'NONE', #25345, #3651, #13724 ) ;
#30351=ORIENTED_EDGE ( 'NONE', *, *, #23923, .T. ) ;
#30373=SURFACE_STYLE_USAGE ( .BOTH. , #16293 ) ;
#30916=( GEOMETRIC_REPRESENTATION_CONTEXT ( 3 ) GLOBAL_UNCERTAINTY_ASSIGNED_CONTEXT ( ( #7606 ) ) GLOBAL_UNIT_ASSIGNED_CONTEXT ( ( #4410, #23890, #28638 ) ) REPRESENTATION_CONTEXT ( 'NONE', 'WORKASPACE' ) );
#30980=ORIENTED_EDGE ( 'NONE', *, *, #8482, .F. ) ;
#31162=DIRECTION ( 'NONE',  ( -1.000000000000000000, 0.000000000000000000, 1.047444401652940007E-14 ) ) ;
#31192=AXIS2_PLACEMENT_3D ( 'NONE', #23774, #11878, #4739 ) ;
#31305=DIRECTION ( 'NONE',  ( 1.015447888376667464E-14, 0.000000000000000000, 1.000000000000000000 ) ) ;
ENDSEC;
END-ISO-10303-21;
